ISO-10303-21;
HEADER;
/* Generated by software containing ST-Developer
 * from STEP Tools, Inc. (www.steptools.com) 
 */

FILE_DESCRIPTION(
/* description */ ('Timing belt drive module 2 mm Pitch Timing 20T-40T'),

/* implementation_level */ '2;1');

FILE_NAME(
/* name */ 'Input M3 set screw (1).step',
/* time_stamp */ '2026-10-28T03:25:12-07:00',
/* author */ (''),
/* organization */ (''),
/* preprocessor_version */ 'ST-DEVELOPER v20.2',
/* originating_system */ 'Autodesk Translation Framework v15.17.0.0',
/* authorisation */ '');

FILE_SCHEMA (('AUTOMOTIVE_DESIGN { 1 0 10303 214 3 1 1 }'));
ENDSEC;

DATA;
#10=MECHANICAL_DESIGN_GEOMETRIC_PRESENTATION_REPRESENTATION('',(#571),#17830);
#470=SHAPE_REPRESENTATION_RELATIONSHIP('SRR','None',#18043,#513);
#513=ADVANCED_BREP_SHAPE_REPRESENTATION('',(#627),#17818);
#571=STYLED_ITEM('',(#18324),#627);
#627=MANIFOLD_SOLID_BREP('Body1',#9030);
#922=PLANE('',#10247);
#923=PLANE('',#10248);
#1286=FACE_OUTER_BOUND('',#1909,.T.);
#1287=FACE_OUTER_BOUND('',#1910,.T.);
#1288=FACE_OUTER_BOUND('',#1911,.T.);
#1909=EDGE_LOOP('',(#7147,#7148,#7149,#7150));
#1910=EDGE_LOOP('',(#7151));
#1911=EDGE_LOOP('',(#7152));
#2496=CIRCLE('',#10245,0.15);
#2497=CIRCLE('',#10246,0.15);
#3089=LINE('',#16041,#3567);
#3567=VECTOR('',#12568,0.15);
#4219=VERTEX_POINT('',#16038);
#4220=VERTEX_POINT('',#16040);
#5256=EDGE_CURVE('',#4219,#4219,#2496,.T.);
#5257=EDGE_CURVE('',#4219,#4220,#3089,.T.);
#5258=EDGE_CURVE('',#4220,#4220,#2497,.T.);
#7147=ORIENTED_EDGE('',*,*,#5256,.F.);
#7148=ORIENTED_EDGE('',*,*,#5257,.T.);
#7149=ORIENTED_EDGE('',*,*,#5258,.T.);
#7150=ORIENTED_EDGE('',*,*,#5257,.F.);
#7151=ORIENTED_EDGE('',*,*,#5256,.T.);
#7152=ORIENTED_EDGE('',*,*,#5258,.F.);
#8307=CYLINDRICAL_SURFACE('',#10244,0.15);
#8784=ADVANCED_FACE('',(#1286),#8307,.T.);
#8785=ADVANCED_FACE('',(#1287),#922,.T.);
#8786=ADVANCED_FACE('',(#1288),#923,.F.);
#9030=CLOSED_SHELL('',(#8784,#8785,#8786));
#10243=AXIS2_PLACEMENT_3D('',#16036,#12562,#12563);
#10244=AXIS2_PLACEMENT_3D('',#16037,#12564,#12565);
#10245=AXIS2_PLACEMENT_3D('',#16039,#12566,#12567);
#10246=AXIS2_PLACEMENT_3D('',#16042,#12569,#12570);
#10247=AXIS2_PLACEMENT_3D('',#16043,#12571,#12572);
#10248=AXIS2_PLACEMENT_3D('',#16044,#12573,#12574);
#12562=DIRECTION('axis',(0.,0.,1.));
#12563=DIRECTION('refdir',(1.,0.,0.));
#12564=DIRECTION('center_axis',(0.,0.,1.));
#12565=DIRECTION('ref_axis',(1.,0.,0.));
#12566=DIRECTION('center_axis',(0.,0.,1.));
#12567=DIRECTION('ref_axis',(1.,0.,0.));
#12568=DIRECTION('',(0.,0.,-1.));
#12569=DIRECTION('center_axis',(0.,0.,1.));
#12570=DIRECTION('ref_axis',(1.,0.,0.));
#12571=DIRECTION('center_axis',(0.,0.,1.));
#12572=DIRECTION('ref_axis',(1.,0.,0.));
#12573=DIRECTION('center_axis',(0.,0.,1.));
#12574=DIRECTION('ref_axis',(1.,0.,0.));
#16036=CARTESIAN_POINT('',(0.,0.,0.));
#16037=CARTESIAN_POINT('Origin',(0.,-3.95,7.4));
#16038=CARTESIAN_POINT('',(-0.15,-3.95,7.65));
#16039=CARTESIAN_POINT('Origin',(0.,-3.95,7.65));
#16040=CARTESIAN_POINT('',(-0.15,-3.95,7.4));
#16041=CARTESIAN_POINT('',(-0.15,-3.95,7.4));
#16042=CARTESIAN_POINT('Origin',(0.,-3.95,7.4));
#16043=CARTESIAN_POINT('Origin',(0.,-3.95,7.65));
#16044=CARTESIAN_POINT('Origin',(0.,-3.95,7.4));
#17768=UNCERTAINTY_MEASURE_WITH_UNIT(LENGTH_MEASURE(0.001),#17831,
'DISTANCE_ACCURACY_VALUE',
'Maximum model space distance between geometric entities at asserted c
onnectivities');
#17780=UNCERTAINTY_MEASURE_WITH_UNIT(LENGTH_MEASURE(0.001),#17831,
'DISTANCE_ACCURACY_VALUE',
'Maximum model space distance between geometric entities at asserted c
onnectivities');
#17818=(
GEOMETRIC_REPRESENTATION_CONTEXT(3)
GLOBAL_UNCERTAINTY_ASSIGNED_CONTEXT((#17768))
GLOBAL_UNIT_ASSIGNED_CONTEXT((#17831,#17833,#17834))
REPRESENTATION_CONTEXT('','3D')
);
#17830=(
GEOMETRIC_REPRESENTATION_CONTEXT(3)
GLOBAL_UNCERTAINTY_ASSIGNED_CONTEXT((#17780))
GLOBAL_UNIT_ASSIGNED_CONTEXT((#17831,#17833,#17834))
REPRESENTATION_CONTEXT('','3D')
);
#17831=(
LENGTH_UNIT()
NAMED_UNIT(*)
SI_UNIT(.CENTI.,.METRE.)
);
#17833=(
NAMED_UNIT(*)
PLANE_ANGLE_UNIT()
SI_UNIT($,.RADIAN.)
);
#17834=(
NAMED_UNIT(*)
SI_UNIT($,.STERADIAN.)
SOLID_ANGLE_UNIT()
);
#17872=SHAPE_DEFINITION_REPRESENTATION(#17931,#18043);
#17931=PRODUCT_DEFINITION_SHAPE('',$,#18093);
#18043=SHAPE_REPRESENTATION('',(#10243),#17818);
#18055=PRODUCT_DEFINITION_CONTEXT('part definition',#18204,'design');
#18093=PRODUCT_DEFINITION('Input M3 set screw (1)',
'Input M3 set screw (1)',#18142,#18055);
#18142=PRODUCT_DEFINITION_FORMATION('',$,#18243);
#18204=APPLICATION_CONTEXT(
'Core Data for Automotive Mechanical Design Process');
#18205=PRODUCT_CONTEXT('part definition',#18204,'mechanical');
#18243=PRODUCT('Input M3 set screw (1)','Input M3 set screw (1)',
'Input M3 set screw (1)',(#18205));
#18318=COLOUR_RGB('Black',0.12,0.14,0.17);
#18319=FILL_AREA_STYLE_COLOUR('',#18318);
#18320=FILL_AREA_STYLE('',(#18319));
#18321=SURFACE_STYLE_FILL_AREA(#18320);
#18322=SURFACE_SIDE_STYLE('',(#18321));
#18323=SURFACE_STYLE_USAGE(.BOTH.,#18322);
#18324=PRESENTATION_STYLE_ASSIGNMENT((#18323));
ENDSEC;
END-ISO-10303-21;
